ISO-10303-21;
HEADER;
/* Generated by software containing ST-Developer
 * from STEP Tools, Inc. (www.steptools.com) 
 */

FILE_DESCRIPTION(
/* description */ (''),
/* implementation_level */ '2;1');

FILE_NAME(
/* name */ 'Bracket_02.step',
/* time_stamp */ '2026-10-22T16:03:28+06:00',
/* author */ (''),
/* organization */ (''),
/* preprocessor_version */ 'ST-DEVELOPER v20.2',
/* originating_system */ 'Autodesk Translation Framework v15.15.0.0',
/* authorisation */ '');

FILE_SCHEMA (('AUTOMOTIVE_DESIGN { 1 0 10303 214 3 1 1 }'));
ENDSEC;

DATA;
#10=MECHANICAL_DESIGN_GEOMETRIC_PRESENTATION_REPRESENTATION('',(#92),#6096);
#70=SHAPE_REPRESENTATION_RELATIONSHIP('SRR','None',#6145,#81);
#81=ADVANCED_BREP_SHAPE_REPRESENTATION('',(#103),#6093);
#92=STYLED_ITEM('',(#6234),#103);
#103=MANIFOLD_SOLID_BREP('Bracket_02',#3601);
#134=FACE_BOUND('',#669,.T.);
#135=FACE_BOUND('',#670,.T.);
#136=FACE_BOUND('',#671,.T.);
#137=FACE_BOUND('',#672,.T.);
#138=FACE_BOUND('',#674,.T.);
#139=FACE_BOUND('',#675,.T.);
#140=FACE_BOUND('',#676,.T.);
#141=FACE_BOUND('',#677,.T.);
#262=PLANE('',#3970);
#263=PLANE('',#3971);
#264=PLANE('',#3972);
#265=PLANE('',#3973);
#266=PLANE('',#3974);
#267=PLANE('',#3975);
#268=PLANE('',#3976);
#269=PLANE('',#3977);
#270=PLANE('',#3978);
#271=PLANE('',#3979);
#272=PLANE('',#3980);
#273=PLANE('',#3981);
#438=FACE_OUTER_BOUND('',#654,.T.);
#439=FACE_OUTER_BOUND('',#655,.T.);
#440=FACE_OUTER_BOUND('',#656,.T.);
#441=FACE_OUTER_BOUND('',#657,.T.);
#442=FACE_OUTER_BOUND('',#658,.T.);
#443=FACE_OUTER_BOUND('',#659,.T.);
#444=FACE_OUTER_BOUND('',#660,.T.);
#445=FACE_OUTER_BOUND('',#661,.T.);
#446=FACE_OUTER_BOUND('',#662,.T.);
#447=FACE_OUTER_BOUND('',#663,.T.);
#448=FACE_OUTER_BOUND('',#664,.T.);
#449=FACE_OUTER_BOUND('',#665,.T.);
#450=FACE_OUTER_BOUND('',#666,.T.);
#451=FACE_OUTER_BOUND('',#667,.T.);
#452=FACE_OUTER_BOUND('',#668,.T.);
#453=FACE_OUTER_BOUND('',#673,.T.);
#654=EDGE_LOOP('',(#3112,#3113,#3114,#3115));
#655=EDGE_LOOP('',(#3116,#3117,#3118,#3119));
#656=EDGE_LOOP('',(#3120,#3121,#3122,#3123));
#657=EDGE_LOOP('',(#3124,#3125,#3126,#3127));
#658=EDGE_LOOP('',(#3128,#3129,#3130,#3131));
#659=EDGE_LOOP('',(#3132,#3133,#3134,#3135));
#660=EDGE_LOOP('',(#3136,#3137,#3138,#3139));
#661=EDGE_LOOP('',(#3140,#3141,#3142,#3143));
#662=EDGE_LOOP('',(#3144,#3145,#3146,#3147));
#663=EDGE_LOOP('',(#3148,#3149,#3150,#3151));
#664=EDGE_LOOP('',(#3152,#3153,#3154,#3155));
#665=EDGE_LOOP('',(#3156,#3157,#3158,#3159));
#666=EDGE_LOOP('',(#3160,#3161,#3162,#3163));
#667=EDGE_LOOP('',(#3164,#3165,#3166,#3167));
#668=EDGE_LOOP('',(#3168,#3169,#3170,#3171,#3172,#3173,#3174,#3175,#3176,
#3177));
#669=EDGE_LOOP('',(#3178));
#670=EDGE_LOOP('',(#3179));
#671=EDGE_LOOP('',(#3180));
#672=EDGE_LOOP('',(#3181));
#673=EDGE_LOOP('',(#3182,#3183,#3184,#3185,#3186,#3187,#3188,#3189,#3190,
#3191));
#674=EDGE_LOOP('',(#3192));
#675=EDGE_LOOP('',(#3193));
#676=EDGE_LOOP('',(#3194));
#677=EDGE_LOOP('',(#3195));
#1003=LINE('',#5804,#1382);
#1004=LINE('',#5810,#1383);
#1005=LINE('',#5816,#1384);
#1006=LINE('',#5822,#1385);
#1007=LINE('',#5827,#1386);
#1008=LINE('',#5829,#1387);
#1009=LINE('',#5831,#1388);
#1010=LINE('',#5832,#1389);
#1011=LINE('',#5835,#1390);
#1012=LINE('',#5837,#1391);
#1013=LINE('',#5838,#1392);
#1014=LINE('',#5841,#1393);
#1015=LINE('',#5843,#1394);
#1016=LINE('',#5844,#1395);
#1017=LINE('',#5847,#1396);
#1018=LINE('',#5849,#1397);
#1019=LINE('',#5850,#1398);
#1020=LINE('',#5853,#1399);
#1021=LINE('',#5855,#1400);
#1022=LINE('',#5856,#1401);
#1023=LINE('',#5859,#1402);
#1024=LINE('',#5861,#1403);
#1025=LINE('',#5862,#1404);
#1026=LINE('',#5865,#1405);
#1027=LINE('',#5867,#1406);
#1028=LINE('',#5868,#1407);
#1029=LINE('',#5871,#1408);
#1030=LINE('',#5873,#1409);
#1031=LINE('',#5874,#1410);
#1032=LINE('',#5877,#1411);
#1033=LINE('',#5879,#1412);
#1034=LINE('',#5880,#1413);
#1035=LINE('',#5882,#1414);
#1036=LINE('',#5883,#1415);
#1382=VECTOR('',#4788,1.99999999999999);
#1383=VECTOR('',#4795,1.99999999999999);
#1384=VECTOR('',#4802,1.99999999999999);
#1385=VECTOR('',#4809,1.99999999999999);
#1386=VECTOR('',#4814,10.);
#1387=VECTOR('',#4815,10.);
#1388=VECTOR('',#4816,10.);
#1389=VECTOR('',#4817,10.);
#1390=VECTOR('',#4820,10.);
#1391=VECTOR('',#4821,10.);
#1392=VECTOR('',#4822,10.);
#1393=VECTOR('',#4825,10.);
#1394=VECTOR('',#4826,10.);
#1395=VECTOR('',#4827,10.);
#1396=VECTOR('',#4830,10.);
#1397=VECTOR('',#4831,10.);
#1398=VECTOR('',#4832,10.);
#1399=VECTOR('',#4835,10.);
#1400=VECTOR('',#4836,10.);
#1401=VECTOR('',#4837,10.);
#1402=VECTOR('',#4840,10.);
#1403=VECTOR('',#4841,10.);
#1404=VECTOR('',#4842,10.);
#1405=VECTOR('',#4845,10.);
#1406=VECTOR('',#4846,10.);
#1407=VECTOR('',#4847,10.);
#1408=VECTOR('',#4850,10.);
#1409=VECTOR('',#4851,10.);
#1410=VECTOR('',#4852,10.);
#1411=VECTOR('',#4855,10.);
#1412=VECTOR('',#4856,10.);
#1413=VECTOR('',#4857,10.);
#1414=VECTOR('',#4860,10.);
#1415=VECTOR('',#4861,10.);
#1566=CIRCLE('',#3959,1.99999999999999);
#1567=CIRCLE('',#3960,1.99999999999999);
#1568=CIRCLE('',#3962,1.99999999999999);
#1569=CIRCLE('',#3963,1.99999999999999);
#1570=CIRCLE('',#3965,1.99999999999999);
#1571=CIRCLE('',#3966,1.99999999999999);
#1572=CIRCLE('',#3968,1.99999999999999);
#1573=CIRCLE('',#3969,1.99999999999999);
#1825=VERTEX_POINT('',#5801);
#1826=VERTEX_POINT('',#5803);
#1827=VERTEX_POINT('',#5807);
#1828=VERTEX_POINT('',#5809);
#1829=VERTEX_POINT('',#5813);
#1830=VERTEX_POINT('',#5815);
#1831=VERTEX_POINT('',#5819);
#1832=VERTEX_POINT('',#5821);
#1833=VERTEX_POINT('',#5825);
#1834=VERTEX_POINT('',#5826);
#1835=VERTEX_POINT('',#5828);
#1836=VERTEX_POINT('',#5830);
#1837=VERTEX_POINT('',#5834);
#1838=VERTEX_POINT('',#5836);
#1839=VERTEX_POINT('',#5840);
#1840=VERTEX_POINT('',#5842);
#1841=VERTEX_POINT('',#5846);
#1842=VERTEX_POINT('',#5848);
#1843=VERTEX_POINT('',#5852);
#1844=VERTEX_POINT('',#5854);
#1845=VERTEX_POINT('',#5858);
#1846=VERTEX_POINT('',#5860);
#1847=VERTEX_POINT('',#5864);
#1848=VERTEX_POINT('',#5866);
#1849=VERTEX_POINT('',#5870);
#1850=VERTEX_POINT('',#5872);
#1851=VERTEX_POINT('',#5876);
#1852=VERTEX_POINT('',#5878);
#2268=EDGE_CURVE('',#1825,#1825,#1566,.T.);
#2269=EDGE_CURVE('',#1825,#1826,#1003,.T.);
#2270=EDGE_CURVE('',#1826,#1826,#1567,.T.);
#2271=EDGE_CURVE('',#1827,#1827,#1568,.T.);
#2272=EDGE_CURVE('',#1827,#1828,#1004,.T.);
#2273=EDGE_CURVE('',#1828,#1828,#1569,.T.);
#2274=EDGE_CURVE('',#1829,#1829,#1570,.T.);
#2275=EDGE_CURVE('',#1829,#1830,#1005,.T.);
#2276=EDGE_CURVE('',#1830,#1830,#1571,.T.);
#2277=EDGE_CURVE('',#1831,#1831,#1572,.T.);
#2278=EDGE_CURVE('',#1831,#1832,#1006,.T.);
#2279=EDGE_CURVE('',#1832,#1832,#1573,.T.);
#2280=EDGE_CURVE('',#1833,#1834,#1007,.T.);
#2281=EDGE_CURVE('',#1833,#1835,#1008,.T.);
#2282=EDGE_CURVE('',#1835,#1836,#1009,.T.);
#2283=EDGE_CURVE('',#1834,#1836,#1010,.T.);
#2284=EDGE_CURVE('',#1837,#1833,#1011,.T.);
#2285=EDGE_CURVE('',#1837,#1838,#1012,.T.);
#2286=EDGE_CURVE('',#1838,#1835,#1013,.T.);
#2287=EDGE_CURVE('',#1839,#1837,#1014,.T.);
#2288=EDGE_CURVE('',#1839,#1840,#1015,.T.);
#2289=EDGE_CURVE('',#1840,#1838,#1016,.T.);
#2290=EDGE_CURVE('',#1841,#1839,#1017,.T.);
#2291=EDGE_CURVE('',#1841,#1842,#1018,.T.);
#2292=EDGE_CURVE('',#1842,#1840,#1019,.T.);
#2293=EDGE_CURVE('',#1843,#1841,#1020,.T.);
#2294=EDGE_CURVE('',#1843,#1844,#1021,.T.);
#2295=EDGE_CURVE('',#1844,#1842,#1022,.T.);
#2296=EDGE_CURVE('',#1845,#1843,#1023,.T.);
#2297=EDGE_CURVE('',#1845,#1846,#1024,.T.);
#2298=EDGE_CURVE('',#1846,#1844,#1025,.T.);
#2299=EDGE_CURVE('',#1847,#1845,#1026,.T.);
#2300=EDGE_CURVE('',#1847,#1848,#1027,.T.);
#2301=EDGE_CURVE('',#1848,#1846,#1028,.T.);
#2302=EDGE_CURVE('',#1849,#1847,#1029,.T.);
#2303=EDGE_CURVE('',#1849,#1850,#1030,.T.);
#2304=EDGE_CURVE('',#1850,#1848,#1031,.T.);
#2305=EDGE_CURVE('',#1851,#1849,#1032,.T.);
#2306=EDGE_CURVE('',#1851,#1852,#1033,.T.);
#2307=EDGE_CURVE('',#1852,#1850,#1034,.T.);
#2308=EDGE_CURVE('',#1834,#1851,#1035,.T.);
#2309=EDGE_CURVE('',#1836,#1852,#1036,.T.);
#3112=ORIENTED_EDGE('',*,*,#2268,.T.);
#3113=ORIENTED_EDGE('',*,*,#2269,.T.);
#3114=ORIENTED_EDGE('',*,*,#2270,.F.);
#3115=ORIENTED_EDGE('',*,*,#2269,.F.);
#3116=ORIENTED_EDGE('',*,*,#2271,.T.);
#3117=ORIENTED_EDGE('',*,*,#2272,.T.);
#3118=ORIENTED_EDGE('',*,*,#2273,.F.);
#3119=ORIENTED_EDGE('',*,*,#2272,.F.);
#3120=ORIENTED_EDGE('',*,*,#2274,.T.);
#3121=ORIENTED_EDGE('',*,*,#2275,.T.);
#3122=ORIENTED_EDGE('',*,*,#2276,.F.);
#3123=ORIENTED_EDGE('',*,*,#2275,.F.);
#3124=ORIENTED_EDGE('',*,*,#2277,.T.);
#3125=ORIENTED_EDGE('',*,*,#2278,.T.);
#3126=ORIENTED_EDGE('',*,*,#2279,.F.);
#3127=ORIENTED_EDGE('',*,*,#2278,.F.);
#3128=ORIENTED_EDGE('',*,*,#2280,.F.);
#3129=ORIENTED_EDGE('',*,*,#2281,.T.);
#3130=ORIENTED_EDGE('',*,*,#2282,.T.);
#3131=ORIENTED_EDGE('',*,*,#2283,.F.);
#3132=ORIENTED_EDGE('',*,*,#2284,.F.);
#3133=ORIENTED_EDGE('',*,*,#2285,.T.);
#3134=ORIENTED_EDGE('',*,*,#2286,.T.);
#3135=ORIENTED_EDGE('',*,*,#2281,.F.);
#3136=ORIENTED_EDGE('',*,*,#2287,.F.);
#3137=ORIENTED_EDGE('',*,*,#2288,.T.);
#3138=ORIENTED_EDGE('',*,*,#2289,.T.);
#3139=ORIENTED_EDGE('',*,*,#2285,.F.);
#3140=ORIENTED_EDGE('',*,*,#2290,.F.);
#3141=ORIENTED_EDGE('',*,*,#2291,.T.);
#3142=ORIENTED_EDGE('',*,*,#2292,.T.);
#3143=ORIENTED_EDGE('',*,*,#2288,.F.);
#3144=ORIENTED_EDGE('',*,*,#2293,.F.);
#3145=ORIENTED_EDGE('',*,*,#2294,.T.);
#3146=ORIENTED_EDGE('',*,*,#2295,.T.);
#3147=ORIENTED_EDGE('',*,*,#2291,.F.);
#3148=ORIENTED_EDGE('',*,*,#2296,.F.);
#3149=ORIENTED_EDGE('',*,*,#2297,.T.);
#3150=ORIENTED_EDGE('',*,*,#2298,.T.);
#3151=ORIENTED_EDGE('',*,*,#2294,.F.);
#3152=ORIENTED_EDGE('',*,*,#2299,.F.);
#3153=ORIENTED_EDGE('',*,*,#2300,.T.);
#3154=ORIENTED_EDGE('',*,*,#2301,.T.);
#3155=ORIENTED_EDGE('',*,*,#2297,.F.);
#3156=ORIENTED_EDGE('',*,*,#2302,.F.);
#3157=ORIENTED_EDGE('',*,*,#2303,.T.);
#3158=ORIENTED_EDGE('',*,*,#2304,.T.);
#3159=ORIENTED_EDGE('',*,*,#2300,.F.);
#3160=ORIENTED_EDGE('',*,*,#2305,.F.);
#3161=ORIENTED_EDGE('',*,*,#2306,.T.);
#3162=ORIENTED_EDGE('',*,*,#2307,.T.);
#3163=ORIENTED_EDGE('',*,*,#2303,.F.);
#3164=ORIENTED_EDGE('',*,*,#2308,.F.);
#3165=ORIENTED_EDGE('',*,*,#2283,.T.);
#3166=ORIENTED_EDGE('',*,*,#2309,.T.);
#3167=ORIENTED_EDGE('',*,*,#2306,.F.);
#3168=ORIENTED_EDGE('',*,*,#2309,.F.);
#3169=ORIENTED_EDGE('',*,*,#2282,.F.);
#3170=ORIENTED_EDGE('',*,*,#2286,.F.);
#3171=ORIENTED_EDGE('',*,*,#2289,.F.);
#3172=ORIENTED_EDGE('',*,*,#2292,.F.);
#3173=ORIENTED_EDGE('',*,*,#2295,.F.);
#3174=ORIENTED_EDGE('',*,*,#2298,.F.);
#3175=ORIENTED_EDGE('',*,*,#2301,.F.);
#3176=ORIENTED_EDGE('',*,*,#2304,.F.);
#3177=ORIENTED_EDGE('',*,*,#2307,.F.);
#3178=ORIENTED_EDGE('',*,*,#2277,.F.);
#3179=ORIENTED_EDGE('',*,*,#2274,.F.);
#3180=ORIENTED_EDGE('',*,*,#2271,.F.);
#3181=ORIENTED_EDGE('',*,*,#2268,.F.);
#3182=ORIENTED_EDGE('',*,*,#2308,.T.);
#3183=ORIENTED_EDGE('',*,*,#2305,.T.);
#3184=ORIENTED_EDGE('',*,*,#2302,.T.);
#3185=ORIENTED_EDGE('',*,*,#2299,.T.);
#3186=ORIENTED_EDGE('',*,*,#2296,.T.);
#3187=ORIENTED_EDGE('',*,*,#2293,.T.);
#3188=ORIENTED_EDGE('',*,*,#2290,.T.);
#3189=ORIENTED_EDGE('',*,*,#2287,.T.);
#3190=ORIENTED_EDGE('',*,*,#2284,.T.);
#3191=ORIENTED_EDGE('',*,*,#2280,.T.);
#3192=ORIENTED_EDGE('',*,*,#2279,.T.);
#3193=ORIENTED_EDGE('',*,*,#2276,.T.);
#3194=ORIENTED_EDGE('',*,*,#2273,.T.);
#3195=ORIENTED_EDGE('',*,*,#2270,.T.);
#3393=CYLINDRICAL_SURFACE('',#3958,1.99999999999999);
#3394=CYLINDRICAL_SURFACE('',#3961,1.99999999999999);
#3395=CYLINDRICAL_SURFACE('',#3964,1.99999999999999);
#3396=CYLINDRICAL_SURFACE('',#3967,1.99999999999999);
#3545=ADVANCED_FACE('',(#438),#3393,.F.);
#3546=ADVANCED_FACE('',(#439),#3394,.F.);
#3547=ADVANCED_FACE('',(#440),#3395,.F.);
#3548=ADVANCED_FACE('',(#441),#3396,.F.);
#3549=ADVANCED_FACE('',(#442),#262,.F.);
#3550=ADVANCED_FACE('',(#443),#263,.F.);
#3551=ADVANCED_FACE('',(#444),#264,.F.);
#3552=ADVANCED_FACE('',(#445),#265,.F.);
#3553=ADVANCED_FACE('',(#446),#266,.F.);
#3554=ADVANCED_FACE('',(#447),#267,.F.);
#3555=ADVANCED_FACE('',(#448),#268,.F.);
#3556=ADVANCED_FACE('',(#449),#269,.F.);
#3557=ADVANCED_FACE('',(#450),#270,.F.);
#3558=ADVANCED_FACE('',(#451),#271,.F.);
#3559=ADVANCED_FACE('',(#452,#134,#135,#136,#137),#272,.F.);
#3560=ADVANCED_FACE('',(#453,#138,#139,#140,#141),#273,.T.);
#3601=CLOSED_SHELL('',(#3545,#3546,#3547,#3548,#3549,#3550,#3551,#3552,
#3553,#3554,#3555,#3556,#3557,#3558,#3559,#3560));
#3957=AXIS2_PLACEMENT_3D('',#5799,#4782,#4783);
#3958=AXIS2_PLACEMENT_3D('',#5800,#4784,#4785);
#3959=AXIS2_PLACEMENT_3D('',#5802,#4786,#4787);
#3960=AXIS2_PLACEMENT_3D('',#5805,#4789,#4790);
#3961=AXIS2_PLACEMENT_3D('',#5806,#4791,#4792);
#3962=AXIS2_PLACEMENT_3D('',#5808,#4793,#4794);
#3963=AXIS2_PLACEMENT_3D('',#5811,#4796,#4797);
#3964=AXIS2_PLACEMENT_3D('',#5812,#4798,#4799);
#3965=AXIS2_PLACEMENT_3D('',#5814,#4800,#4801);
#3966=AXIS2_PLACEMENT_3D('',#5817,#4803,#4804);
#3967=AXIS2_PLACEMENT_3D('',#5818,#4805,#4806);
#3968=AXIS2_PLACEMENT_3D('',#5820,#4807,#4808);
#3969=AXIS2_PLACEMENT_3D('',#5823,#4810,#4811);
#3970=AXIS2_PLACEMENT_3D('',#5824,#4812,#4813);
#3971=AXIS2_PLACEMENT_3D('',#5833,#4818,#4819);
#3972=AXIS2_PLACEMENT_3D('',#5839,#4823,#4824);
#3973=AXIS2_PLACEMENT_3D('',#5845,#4828,#4829);
#3974=AXIS2_PLACEMENT_3D('',#5851,#4833,#4834);
#3975=AXIS2_PLACEMENT_3D('',#5857,#4838,#4839);
#3976=AXIS2_PLACEMENT_3D('',#5863,#4843,#4844);
#3977=AXIS2_PLACEMENT_3D('',#5869,#4848,#4849);
#3978=AXIS2_PLACEMENT_3D('',#5875,#4853,#4854);
#3979=AXIS2_PLACEMENT_3D('',#5881,#4858,#4859);
#3980=AXIS2_PLACEMENT_3D('',#5884,#4862,#4863);
#3981=AXIS2_PLACEMENT_3D('',#5885,#4864,#4865);
#4782=DIRECTION('axis',(0.,0.,1.));
#4783=DIRECTION('refdir',(1.,0.,0.));
#4784=DIRECTION('center_axis',(0.,1.,0.));
#4785=DIRECTION('ref_axis',(-1.,0.,0.));
#4786=DIRECTION('center_axis',(0.,-1.,0.));
#4787=DIRECTION('ref_axis',(-1.,0.,0.));
#4788=DIRECTION('',(0.,1.,0.));
#4789=DIRECTION('center_axis',(0.,-1.,0.));
#4790=DIRECTION('ref_axis',(-1.,0.,0.));
#4791=DIRECTION('center_axis',(0.,1.,0.));
#4792=DIRECTION('ref_axis',(-1.,0.,0.));
#4793=DIRECTION('center_axis',(0.,-1.,0.));
#4794=DIRECTION('ref_axis',(-1.,0.,0.));
#4795=DIRECTION('',(0.,1.,0.));
#4796=DIRECTION('center_axis',(0.,-1.,0.));
#4797=DIRECTION('ref_axis',(-1.,0.,0.));
#4798=DIRECTION('center_axis',(0.,1.,0.));
#4799=DIRECTION('ref_axis',(-1.,0.,0.));
#4800=DIRECTION('center_axis',(0.,-1.,0.));
#4801=DIRECTION('ref_axis',(-1.,0.,0.));
#4802=DIRECTION('',(0.,1.,0.));
#4803=DIRECTION('center_axis',(0.,-1.,0.));
#4804=DIRECTION('ref_axis',(-1.,0.,0.));
#4805=DIRECTION('center_axis',(0.,1.,0.));
#4806=DIRECTION('ref_axis',(-1.,0.,0.));
#4807=DIRECTION('center_axis',(0.,-1.,0.));
#4808=DIRECTION('ref_axis',(-1.,0.,0.));
#4809=DIRECTION('',(0.,1.,0.));
#4810=DIRECTION('center_axis',(0.,-1.,0.));
#4811=DIRECTION('ref_axis',(-1.,0.,0.));
#4812=DIRECTION('center_axis',(0.,0.,1.));
#4813=DIRECTION('ref_axis',(-1.,0.,0.));
#4814=DIRECTION('',(-1.,0.,0.));
#4815=DIRECTION('',(0.,-1.,0.));
#4816=DIRECTION('',(-1.,0.,0.));
#4817=DIRECTION('',(0.,-1.,0.));
#4818=DIRECTION('center_axis',(1.,0.,0.));
#4819=DIRECTION('ref_axis',(0.,0.,1.));
#4820=DIRECTION('',(0.,0.,1.));
#4821=DIRECTION('',(0.,-1.,0.));
#4822=DIRECTION('',(0.,0.,1.));
#4823=DIRECTION('center_axis',(0.,0.,-1.));
#4824=DIRECTION('ref_axis',(1.,0.,0.));
#4825=DIRECTION('',(1.,0.,0.));
#4826=DIRECTION('',(0.,-1.,0.));
#4827=DIRECTION('',(1.,0.,0.));
#4828=DIRECTION('center_axis',(1.,0.,0.));
#4829=DIRECTION('ref_axis',(0.,0.,1.));
#4830=DIRECTION('',(0.,0.,1.));
#4831=DIRECTION('',(0.,-1.,0.));
#4832=DIRECTION('',(0.,0.,1.));
#4833=DIRECTION('center_axis',(0.,0.,1.));
#4834=DIRECTION('ref_axis',(-1.,0.,0.));
#4835=DIRECTION('',(-1.,0.,0.));
#4836=DIRECTION('',(0.,-1.,0.));
#4837=DIRECTION('',(-1.,0.,0.));
#4838=DIRECTION('center_axis',(-1.,0.,0.));
#4839=DIRECTION('ref_axis',(0.,0.,-1.));
#4840=DIRECTION('',(0.,0.,-1.));
#4841=DIRECTION('',(0.,-1.,0.));
#4842=DIRECTION('',(0.,0.,-1.));
#4843=DIRECTION('center_axis',(0.,0.,-1.));
#4844=DIRECTION('ref_axis',(1.,0.,0.));
#4845=DIRECTION('',(1.,0.,0.));
#4846=DIRECTION('',(0.,-1.,0.));
#4847=DIRECTION('',(1.,0.,0.));
#4848=DIRECTION('center_axis',(1.,0.,0.));
#4849=DIRECTION('ref_axis',(0.,0.,1.));
#4850=DIRECTION('',(0.,0.,1.));
#4851=DIRECTION('',(0.,-1.,0.));
#4852=DIRECTION('',(0.,0.,1.));
#4853=DIRECTION('center_axis',(0.,0.,1.));
#4854=DIRECTION('ref_axis',(-1.,0.,0.));
#4855=DIRECTION('',(-1.,0.,0.));
#4856=DIRECTION('',(0.,-1.,0.));
#4857=DIRECTION('',(-1.,0.,0.));
#4858=DIRECTION('center_axis',(-1.,0.,0.));
#4859=DIRECTION('ref_axis',(0.,0.,-1.));
#4860=DIRECTION('',(0.,0.,-1.));
#4861=DIRECTION('',(0.,0.,-1.));
#4862=DIRECTION('center_axis',(0.,1.,0.));
#4863=DIRECTION('ref_axis',(-1.,0.,0.));
#4864=DIRECTION('center_axis',(0.,1.,0.));
#4865=DIRECTION('ref_axis',(-1.,0.,0.));
#5799=CARTESIAN_POINT('',(0.,0.,0.));
#5800=CARTESIAN_POINT('Origin',(31.6092837386808,245.5,108.939950998448));
#5801=CARTESIAN_POINT('',(33.6092837386808,242.5,108.939950998448));
#5802=CARTESIAN_POINT('Origin',(31.6092837386808,242.5,108.939950998448));
#5803=CARTESIAN_POINT('',(33.6092837386808,245.5,108.939950998448));
#5804=CARTESIAN_POINT('',(33.6092837386808,245.5,108.939950998448));
#5805=CARTESIAN_POINT('Origin',(31.6092837386808,245.5,108.939950998448));
#5806=CARTESIAN_POINT('Origin',(71.0061608111161,245.5,95.0000000000015));
#5807=CARTESIAN_POINT('',(73.0061608111161,242.5,95.0000000000015));
#5808=CARTESIAN_POINT('Origin',(71.0061608111161,242.5,95.0000000000015));
#5809=CARTESIAN_POINT('',(73.0061608111161,245.5,95.0000000000015));
#5810=CARTESIAN_POINT('',(73.0061608111161,245.5,95.0000000000015));
#5811=CARTESIAN_POINT('Origin',(71.0061608111161,245.5,95.0000000000015));
#5812=CARTESIAN_POINT('Origin',(28.0061608111161,245.5,95.0000000000015));
#5813=CARTESIAN_POINT('',(30.0061608111161,242.5,95.0000000000015));
#5814=CARTESIAN_POINT('Origin',(28.0061608111161,242.5,95.0000000000015));
#5815=CARTESIAN_POINT('',(30.0061608111161,245.5,95.0000000000015));
#5816=CARTESIAN_POINT('',(30.0061608111161,245.5,95.0000000000015));
#5817=CARTESIAN_POINT('Origin',(28.0061608111161,245.5,95.0000000000015));
#5818=CARTESIAN_POINT('Origin',(67.4030378835514,245.5,108.939950998448));
#5819=CARTESIAN_POINT('',(69.4030378835514,242.5,108.939950998448));
#5820=CARTESIAN_POINT('Origin',(67.4030378835514,242.5,108.939950998448));
#5821=CARTESIAN_POINT('',(69.4030378835514,245.5,108.939950998448));
#5822=CARTESIAN_POINT('',(69.4030378835514,245.5,108.939950998448));
#5823=CARTESIAN_POINT('Origin',(67.4030378835514,245.5,108.939950998448));
#5824=CARTESIAN_POINT('Origin',(67.5061608111161,245.5,105.000000000001));
#5825=CARTESIAN_POINT('',(67.5061608111161,245.5,105.000000000001));
#5826=CARTESIAN_POINT('',(31.5061608111161,245.5,105.000000000001));
#5827=CARTESIAN_POINT('',(67.5061608111161,245.5,105.000000000001));
#5828=CARTESIAN_POINT('',(67.5061608111161,242.5,105.000000000001));
#5829=CARTESIAN_POINT('',(67.5061608111161,245.5,105.000000000001));
#5830=CARTESIAN_POINT('',(31.5061608111161,242.5,105.000000000001));
#5831=CARTESIAN_POINT('',(67.5061608111161,242.5,105.000000000001));
#5832=CARTESIAN_POINT('',(31.5061608111161,245.5,105.000000000001));
#5833=CARTESIAN_POINT('Origin',(67.5061608111161,245.5,85.0000000000015));
#5834=CARTESIAN_POINT('',(67.5061608111161,245.5,85.0000000000015));
#5835=CARTESIAN_POINT('',(67.5061608111161,245.5,85.0000000000015));
#5836=CARTESIAN_POINT('',(67.5061608111161,242.5,85.0000000000015));
#5837=CARTESIAN_POINT('',(67.5061608111161,245.5,85.0000000000015));
#5838=CARTESIAN_POINT('',(67.5061608111161,242.5,85.0000000000015));
#5839=CARTESIAN_POINT('Origin',(51.5061608111161,245.5,85.0000000000015));
#5840=CARTESIAN_POINT('',(51.5061608111161,245.5,85.0000000000015));
#5841=CARTESIAN_POINT('',(31.5061608111161,245.5,85.0000000000015));
#5842=CARTESIAN_POINT('',(51.5061608111161,242.5,85.0000000000015));
#5843=CARTESIAN_POINT('',(51.5061608111161,245.5,85.0000000000015));
#5844=CARTESIAN_POINT('',(31.5061608111161,242.5,85.0000000000015));
#5845=CARTESIAN_POINT('Origin',(51.5061608111161,245.5,77.5000000000015));
#5846=CARTESIAN_POINT('',(51.5061608111161,245.5,77.5000000000015));
#5847=CARTESIAN_POINT('',(51.5061608111161,245.5,65.0000000000015));
#5848=CARTESIAN_POINT('',(51.5061608111161,242.5,77.5000000000015));
#5849=CARTESIAN_POINT('',(51.5061608111161,245.5,77.5000000000015));
#5850=CARTESIAN_POINT('',(51.5061608111161,242.5,65.0000000000015));
#5851=CARTESIAN_POINT('Origin',(74.5061608111161,245.5,77.5000000000015));
#5852=CARTESIAN_POINT('',(74.5061608111161,245.5,77.5000000000015));
#5853=CARTESIAN_POINT('',(74.5061608111161,245.5,77.5000000000015));
#5854=CARTESIAN_POINT('',(74.5061608111161,242.5,77.5000000000015));
#5855=CARTESIAN_POINT('',(74.5061608111161,245.5,77.5000000000015));
#5856=CARTESIAN_POINT('',(74.5061608111161,242.5,77.5000000000015));
#5857=CARTESIAN_POINT('Origin',(74.5061608111161,245.5,112.500000000001));
#5858=CARTESIAN_POINT('',(74.5061608111161,245.5,112.500000000001));
#5859=CARTESIAN_POINT('',(74.5061608111161,245.5,112.500000000001));
#5860=CARTESIAN_POINT('',(74.5061608111161,242.5,112.500000000001));
#5861=CARTESIAN_POINT('',(74.5061608111161,245.5,112.500000000001));
#5862=CARTESIAN_POINT('',(74.5061608111161,242.5,112.500000000001));
#5863=CARTESIAN_POINT('Origin',(24.5061608111161,245.5,112.500000000001));
#5864=CARTESIAN_POINT('',(24.5061608111161,245.5,112.500000000001));
#5865=CARTESIAN_POINT('',(24.5061608111161,245.5,112.500000000001));
#5866=CARTESIAN_POINT('',(24.5061608111161,242.5,112.500000000001));
#5867=CARTESIAN_POINT('',(24.5061608111161,245.5,112.500000000001));
#5868=CARTESIAN_POINT('',(24.5061608111161,242.5,112.500000000001));
#5869=CARTESIAN_POINT('Origin',(24.5061608111161,245.5,77.5000000000015));
#5870=CARTESIAN_POINT('',(24.5061608111161,245.5,77.5000000000015));
#5871=CARTESIAN_POINT('',(24.5061608111161,245.5,77.5000000000015));
#5872=CARTESIAN_POINT('',(24.5061608111161,242.5,77.5000000000015));
#5873=CARTESIAN_POINT('',(24.5061608111161,245.5,77.5000000000015));
#5874=CARTESIAN_POINT('',(24.5061608111161,242.5,77.5000000000015));
#5875=CARTESIAN_POINT('Origin',(31.5061608111161,245.5,77.5000000000015));
#5876=CARTESIAN_POINT('',(31.5061608111161,245.5,77.5000000000015));
#5877=CARTESIAN_POINT('',(74.5061608111161,245.5,77.5000000000015));
#5878=CARTESIAN_POINT('',(31.5061608111161,242.5,77.5000000000015));
#5879=CARTESIAN_POINT('',(31.5061608111161,245.5,77.5000000000015));
#5880=CARTESIAN_POINT('',(74.5061608111161,242.5,77.5000000000015));
#5881=CARTESIAN_POINT('Origin',(31.5061608111161,245.5,105.000000000001));
#5882=CARTESIAN_POINT('',(31.5061608111161,245.5,85.0000000000015));
#5883=CARTESIAN_POINT('',(31.5061608111161,242.5,85.0000000000015));
#5884=CARTESIAN_POINT('Origin',(49.5061608111161,242.5,95.0000000000015));
#5885=CARTESIAN_POINT('Origin',(49.5061608111161,245.5,95.0000000000015));
#6080=UNCERTAINTY_MEASURE_WITH_UNIT(LENGTH_MEASURE(0.01),#6097,
'DISTANCE_ACCURACY_VALUE',
'Maximum model space distance between geometric entities at asserted c
onnectivities');
#6083=UNCERTAINTY_MEASURE_WITH_UNIT(LENGTH_MEASURE(0.01),#6097,
'DISTANCE_ACCURACY_VALUE',
'Maximum model space distance between geometric entities at asserted c
onnectivities');
#6093=(
GEOMETRIC_REPRESENTATION_CONTEXT(3)
GLOBAL_UNCERTAINTY_ASSIGNED_CONTEXT((#6080))
GLOBAL_UNIT_ASSIGNED_CONTEXT((#6097,#6099,#6100))
REPRESENTATION_CONTEXT('','3D')
);
#6096=(
GEOMETRIC_REPRESENTATION_CONTEXT(3)
GLOBAL_UNCERTAINTY_ASSIGNED_CONTEXT((#6083))
GLOBAL_UNIT_ASSIGNED_CONTEXT((#6097,#6099,#6100))
REPRESENTATION_CONTEXT('','3D')
);
#6097=(
LENGTH_UNIT()
NAMED_UNIT(*)
SI_UNIT(.MILLI.,.METRE.)
);
#6099=(
NAMED_UNIT(*)
PLANE_ANGLE_UNIT()
SI_UNIT($,.RADIAN.)
);
#6100=(
NAMED_UNIT(*)
SI_UNIT($,.STERADIAN.)
SOLID_ANGLE_UNIT()
);
#6110=SHAPE_DEFINITION_REPRESENTATION(#6122,#6145);
#6122=PRODUCT_DEFINITION_SHAPE('',$,#6158);
#6145=SHAPE_REPRESENTATION('',(#3957),#6093);
#6148=PRODUCT_DEFINITION_CONTEXT('part definition',#6186,'design');
#6158=PRODUCT_DEFINITION('Bracket_02','Bracket_02',#6170,#6148);
#6170=PRODUCT_DEFINITION_FORMATION('',$,#6197);
#6186=APPLICATION_CONTEXT(
'Core Data for Automotive Mechanical Design Process');
#6187=PRODUCT_CONTEXT('part definition',#6186,'mechanical');
#6197=PRODUCT('Bracket_02','Bracket_02',$,(#6187));
#6228=COLOUR_RGB('Dark Blue',0.08,0.2,0.34);
#6229=FILL_AREA_STYLE_COLOUR('',#6228);
#6230=FILL_AREA_STYLE('',(#6229));
#6231=SURFACE_STYLE_FILL_AREA(#6230);
#6232=SURFACE_SIDE_STYLE('',(#6231));
#6233=SURFACE_STYLE_USAGE(.BOTH.,#6232);
#6234=PRESENTATION_STYLE_ASSIGNMENT((#6233));
ENDSEC;
END-ISO-10303-21;
